ISO-10303-21;
HEADER;
FILE_DESCRIPTION (('STEP AP214'),
    '1' );
FILE_NAME ('Pin 4X6.step',
    '2026-10-22T18:53:08',
    ( '' ),
    ( '' ),
    'SwSTEP 2.0',
    'SolidWorks 2025',
    '' );
FILE_SCHEMA (( 'AUTOMOTIVE_DESIGN' ));
ENDSEC;

DATA;
#65=CARTESIAN_POINT ( 'NONE',  ( 1.499999999999998668, 0.000000000000000000, 0.000000000000000000 ) ) ;
#181=AXIS2_PLACEMENT_3D ( 'NONE', #13269, #18906, #9720 ) ;
#335=DIRECTION ( 'NONE',  ( 1.000000000000000000, 0.000000000000000000, -0.000000000000000000 ) ) ;
#363=DIRECTION ( 'NONE',  ( 0.000000000000000000, 0.000000000000000000, -1.000000000000000000 ) ) ;
#365=ADVANCED_FACE ( 'NONE', ( #20098 ), #2718, .T. ) ;
#447=DIRECTION ( 'NONE',  ( 0.000000000000000000, 0.000000000000000000, 1.000000000000000000 ) ) ;
#457=ORIENTED_EDGE ( 'NONE', *, *, #5013, .F. ) ;
#503=ADVANCED_FACE ( 'NONE', ( #16404 ), #10677, .T. ) ;
#554=CIRCLE ( 'NONE', #181, 1.499999999999999556 ) ;
#565=FACE_OUTER_BOUND ( 'NONE', #11351, .T. ) ;
#581=VERTEX_POINT ( 'NONE', #8030 ) ;
#601=STYLED_ITEM('',(#24155),#2929);
#780=VERTEX_POINT ( 'NONE', #13683 ) ;
#806=ORIENTED_EDGE ( 'NONE', *, *, #11080, .F. ) ;
#888=DIRECTION ( 'NONE',  ( -0.7071067811865489050, 8.659560562354950115E-17, 0.7071067811865462405 ) ) ;
#1078=EDGE_CURVE ( 'NONE', #780, #10236, #16463, .T. ) ;
#1090=DIRECTION ( 'NONE',  ( 0.000000000000000000, 0.000000000000000000, 1.000000000000000000 ) ) ;
#1148=CARTESIAN_POINT ( 'NONE',  ( -2.000000000000000000, 0.000000000000000000, 6.000000000000000000 ) ) ;
#1237=CARTESIAN_POINT ( 'NONE',  ( 0.000000000000000000, 0.000000000000000000, 5.499999999999997335 ) ) ;
#1370=AXIS2_PLACEMENT_3D ( 'NONE', #19005, #447, #335 ) ;
#1375=ORIENTED_EDGE ( 'NONE', *, *, #3223, .T. ) ;
#1399=DIRECTION ( 'NONE',  ( -1.000000000000000000, 0.000000000000000000, 0.000000000000000000 ) ) ;
#1431=PRODUCT_DEFINITION ( 'UNKNOWN', '', #16228, #4583 ) ;
#1496=ORIENTED_EDGE ( 'NONE', *, *, #15252, .F. ) ;
#1555=CARTESIAN_POINT ( 'NONE',  ( -1.499999999999999556, 0.000000000000000000, 6.000000000000000000 ) ) ;
#1771=VECTOR ( 'NONE', #888, 999.9999999999998863 ) ;
#1779=AXIS2_PLACEMENT_3D ( 'NONE', #12915, #363, #7772 ) ;
#1820=SHAPE_REPRESENTATION_RELATIONSHIP ( 'NONE' , 'NONE' ,  #15290, #22430 ) ;
#1827=( NAMED_UNIT ( * ) PLANE_ANGLE_UNIT ( ) SI_UNIT ( $, .RADIAN. ) );
#1936=CARTESIAN_POINT ( 'NONE',  ( 2.000000000000000000, 2.449293598294706414E-16, 6.000000000000000000 ) ) ;
#1940=ORIENTED_EDGE ( 'NONE', *, *, #14691, .T. ) ;
#1981=EDGE_CURVE ( 'NONE', #14771, #780, #17731, .T. ) ;
#2144=CARTESIAN_POINT ( 'NONE',  ( 0.000000000000000000, 0.000000000000000000, 6.000000000000000000 ) ) ;
#2496=ORIENTED_EDGE ( 'NONE', *, *, #3201, .F. ) ;
#2614=FACE_OUTER_BOUND ( 'NONE', #7953, .T. ) ;
#2718=CONICAL_SURFACE ( 'NONE', #8514, 2.000000000000000000, 0.7853981633974501664 ) ;
#2827=CONICAL_SURFACE ( 'NONE', #23085, 2.000000000000000000, 0.7853981633974501664 ) ;
#2929=MANIFOLD_SOLID_BREP ( 'Chamfer1', #8111 ) ;
#3201=EDGE_CURVE ( 'NONE', #10964, #3333, #6455, .T. ) ;
#3223=EDGE_CURVE ( 'NONE', #17567, #10236, #6811, .T. ) ;
#3332=MECHANICAL_DESIGN_GEOMETRIC_PRESENTATION_REPRESENTATION('',(#601),#16184);
#3333=VERTEX_POINT ( 'NONE', #1555 ) ;
#3344=ORIENTED_EDGE ( 'NONE', *, *, #1981, .T. ) ;
#3416=PRODUCT ( 'Pin 4X6', 'Pin 4X6', '', ( #15053 ) ) ;
#3470=EDGE_LOOP ( 'NONE', ( #457, #7724, #8218, #16655 ) ) ;
#3642=ADVANCED_FACE ( 'NONE', ( #565 ), #18864, .T. ) ;
#3708=CIRCLE ( 'NONE', #20441, 1.499999999999998668 ) ;
#3730=ORIENTED_EDGE ( 'NONE', *, *, #5013, .T. ) ;
#3868=FACE_OUTER_BOUND ( 'NONE', #15410, .T. ) ;
#4108=DIRECTION ( 'NONE',  ( -1.000000000000000000, 0.000000000000000000, 0.000000000000000000 ) ) ;
#4583=PRODUCT_DEFINITION_CONTEXT ( 'detailed design', #6978, 'design' ) ;
#4665=CARTESIAN_POINT ( 'NONE',  ( -1.499999999999998668, 2.143131898507867311E-16, 0.000000000000000000 ) ) ;
#4690=DIRECTION ( 'NONE',  ( 0.000000000000000000, 0.000000000000000000, -1.000000000000000000 ) ) ;
#5013=EDGE_CURVE ( 'NONE', #10964, #581, #19283, .T. ) ;
#5297=ORIENTED_EDGE ( 'NONE', *, *, #10265, .F. ) ;
#5538=DIRECTION ( 'NONE',  ( -0.7071067811865456854, 0.000000000000000000, -0.7071067811865493491 ) ) ;
#5562=CYLINDRICAL_SURFACE ( 'NONE', #19744, 2.000000000000000000 ) ;
#5601=( LENGTH_UNIT ( ) NAMED_UNIT ( * ) SI_UNIT ( .MILLI., .METRE. ) );
#5921=DIRECTION ( 'NONE',  ( -1.000000000000000000, 0.000000000000000000, 0.000000000000000000 ) ) ;
#5923=CARTESIAN_POINT ( 'NONE',  ( 0.000000000000000000, 0.000000000000000000, 6.000000000000000000 ) ) ;
#5955=AXIS2_PLACEMENT_3D ( 'NONE', #7781, #22571, #14994 ) ;
#5978=CARTESIAN_POINT ( 'NONE',  ( 0.000000000000000000, 0.000000000000000000, 0.000000000000000000 ) ) ;
#5979=CARTESIAN_POINT ( 'NONE',  ( 1.499999999999999556, 1.836970198721029441E-16, 6.000000000000000000 ) ) ;
#6014=LINE ( 'NONE', #19071, #1771 ) ;
#6254=ADVANCED_FACE ( 'NONE', ( #19705 ), #20031, .T. ) ;
#6285=AXIS2_PLACEMENT_3D ( 'NONE', #12770, #18634, #10809 ) ;
#6455=CIRCLE ( 'NONE', #22049, 1.499999999999999556 ) ;
#6637=CARTESIAN_POINT ( 'NONE',  ( 0.000000000000000000, 0.000000000000000000, 0.4999999999999995559 ) ) ;
#6747=AXIS2_PLACEMENT_3D ( 'NONE', #1237, #24035, #14750 ) ;
#6811=LINE ( 'NONE', #14237, #7315 ) ;
#6918=PRODUCT_DEFINITION_SHAPE ( 'NONE', 'NONE',  #1431 ) ;
#6978=APPLICATION_CONTEXT ( 'automotive_design' ) ;
#7008=DIRECTION ( 'NONE',  ( 1.000000000000000000, 0.000000000000000000, 0.000000000000000000 ) ) ;
#7129=CARTESIAN_POINT ( 'NONE',  ( -1.499999999999999556, 0.000000000000000000, 6.000000000000000000 ) ) ;
#7145=DIRECTION ( 'NONE',  ( -0.000000000000000000, -0.000000000000000000, 1.000000000000000000 ) ) ;
#7315=VECTOR ( 'NONE', #21699, 999.9999999999998863 ) ;
#7377=DIRECTION ( 'NONE',  ( -0.000000000000000000, -0.000000000000000000, -1.000000000000000000 ) ) ;
#7724=ORIENTED_EDGE ( 'NONE', *, *, #20306, .F. ) ;
#7772=DIRECTION ( 'NONE',  ( -1.000000000000000000, 0.000000000000000000, 0.000000000000000000 ) ) ;
#7781=CARTESIAN_POINT ( 'NONE',  ( 0.000000000000000000, 0.000000000000000000, 0.4999999999999995559 ) ) ;
#7897=EDGE_LOOP ( 'NONE', ( #15539, #13316, #23120, #8827 ) ) ;
#7953=EDGE_LOOP ( 'NONE', ( #18910, #1496, #1375, #9414 ) ) ;
#8005=AXIS2_PLACEMENT_3D ( 'NONE', #5978, #22344, #13412 ) ;
#8030=CARTESIAN_POINT ( 'NONE',  ( 2.000000000000000000, 2.449293598294706414E-16, 5.499999999999997335 ) ) ;
#8111=CLOSED_SHELL ( 'NONE', ( #13261, #365, #23525, #3642, #503, #17102, #11269, #6254 ) ) ;
#8157=ORIENTED_EDGE ( 'NONE', *, *, #14691, .F. ) ;
#8218=ORIENTED_EDGE ( 'NONE', *, *, #11080, .T. ) ;
#8221=EDGE_CURVE ( 'NONE', #581, #14771, #20377, .T. ) ;
#8357=DIRECTION ( 'NONE',  ( -0.000000000000000000, -0.000000000000000000, -1.000000000000000000 ) ) ;
#8514=AXIS2_PLACEMENT_3D ( 'NONE', #20216, #7145, #14450 ) ;
#8615=DIRECTION ( 'NONE',  ( 1.000000000000000000, 0.000000000000000000, 0.000000000000000000 ) ) ;
#8690=EDGE_LOOP ( 'NONE', ( #8157, #19943, #20750, #14632 ) ) ;
#8732=ORIENTED_EDGE ( 'NONE', *, *, #20306, .T. ) ;
#8827=ORIENTED_EDGE ( 'NONE', *, *, #1981, .F. ) ;
#9073=CIRCLE ( 'NONE', #13758, 2.000000000000000000 ) ;
#9182=AXIS2_PLACEMENT_3D ( 'NONE', #23739, #8357, #7008 ) ;
#9253=LINE ( 'NONE', #1936, #16819 ) ;
#9343=( NAMED_UNIT ( * ) SI_UNIT ( $, .STERADIAN. ) SOLID_ANGLE_UNIT ( ) );
#9414=ORIENTED_EDGE ( 'NONE', *, *, #1078, .F. ) ;
#9615=FACE_OUTER_BOUND ( 'NONE', #10535, .T. ) ;
#9720=DIRECTION ( 'NONE',  ( 1.000000000000000000, 0.000000000000000000, 0.000000000000000000 ) ) ;
#9905=EDGE_CURVE ( 'NONE', #14771, #581, #9073, .T. ) ;
#10236=VERTEX_POINT ( 'NONE', #14749 ) ;
#10265=EDGE_CURVE ( 'NONE', #581, #10236, #9253, .T. ) ;
#10409=DIRECTION ( 'NONE',  ( 1.000000000000000000, 0.000000000000000000, 0.000000000000000000 ) ) ;
#10532=ORIENTED_EDGE ( 'NONE', *, *, #15252, .T. ) ;
#10535=EDGE_LOOP ( 'NONE', ( #2496, #3730, #11489, #806 ) ) ;
#10677=PLANE ( 'NONE',  #17072 ) ;
#10720=EDGE_CURVE ( 'NONE', #10236, #780, #16789, .T. ) ;
#10809=DIRECTION ( 'NONE',  ( 1.000000000000000000, 0.000000000000000000, 0.000000000000000000 ) ) ;
#10964=VERTEX_POINT ( 'NONE', #19603 ) ;
#11080=EDGE_CURVE ( 'NONE', #3333, #14771, #18480, .T. ) ;
#11211=CARTESIAN_POINT ( 'NONE',  ( 0.000000000000000000, 0.000000000000000000, 5.499999999999997335 ) ) ;
#11269=ADVANCED_FACE ( 'NONE', ( #2614 ), #2827, .T. ) ;
#11274=PLANE ( 'NONE',  #1370 ) ;
#11351=EDGE_LOOP ( 'NONE', ( #5297, #16921, #3344, #12191 ) ) ;
#11489=ORIENTED_EDGE ( 'NONE', *, *, #9905, .F. ) ;
#12053=CARTESIAN_POINT ( 'NONE',  ( -2.000000000000000000, 0.000000000000000000, 5.499999999999997335 ) ) ;
#12191=ORIENTED_EDGE ( 'NONE', *, *, #1078, .T. ) ;
#12290=CONICAL_SURFACE ( 'NONE', #1779, 1.499999999999999556, 0.7853981633974457255 ) ;
#12770=CARTESIAN_POINT ( 'NONE',  ( 0.000000000000000000, 0.000000000000000000, 0.4999999999999995559 ) ) ;
#12896=( NAMED_UNIT ( * ) PLANE_ANGLE_UNIT ( ) SI_UNIT ( $, .RADIAN. ) );
#12915=CARTESIAN_POINT ( 'NONE',  ( 0.000000000000000000, 0.000000000000000000, 6.000000000000000000 ) ) ;
#12916=VERTEX_POINT ( 'NONE', #4665 ) ;
#13169=VECTOR ( 'NONE', #18103, 1000.000000000000000 ) ;
#13261=ADVANCED_FACE ( 'NONE', ( #9615 ), #12290, .T. ) ;
#13269=CARTESIAN_POINT ( 'NONE',  ( 0.000000000000000000, 0.000000000000000000, 6.000000000000000000 ) ) ;
#13316=ORIENTED_EDGE ( 'NONE', *, *, #10265, .T. ) ;
#13412=DIRECTION ( 'NONE',  ( 1.000000000000000000, 0.000000000000000000, 0.000000000000000000 ) ) ;
#13522=UNCERTAINTY_MEASURE_WITH_UNIT (LENGTH_MEASURE( 1.000000000000000082E-05 ), #20478, 'distance_accuracy_value', 'NONE');
#13683=CARTESIAN_POINT ( 'NONE',  ( -2.000000000000000000, 0.000000000000000000, 0.4999999999999995559 ) ) ;
#13708=EDGE_LOOP ( 'NONE', ( #8732, #18578 ) ) ;
#13758=AXIS2_PLACEMENT_3D ( 'NONE', #11211, #18134, #23844 ) ;
#13887=( GEOMETRIC_REPRESENTATION_CONTEXT ( 3 ) GLOBAL_UNCERTAINTY_ASSIGNED_CONTEXT ( ( #13522 ) ) GLOBAL_UNIT_ASSIGNED_CONTEXT ( ( #20478, #12896, #9343 ) ) REPRESENTATION_CONTEXT ( 'NONE', 'WORKASPACE' ) );
#14007=CARTESIAN_POINT ( 'NONE',  ( 0.000000000000000000, 0.000000000000000000, 6.000000000000000000 ) ) ;
#14237=CARTESIAN_POINT ( 'NONE',  ( 2.000000000000000000, 0.000000000000000000, 0.4999999999999995559 ) ) ;
#14450=DIRECTION ( 'NONE',  ( 1.000000000000000000, 0.000000000000000000, 0.000000000000000000 ) ) ;
#14581=CARTESIAN_POINT ( 'NONE',  ( 0.000000000000000000, 0.000000000000000000, 6.000000000000000000 ) ) ;
#14632=ORIENTED_EDGE ( 'NONE', *, *, #3223, .F. ) ;
#14691=EDGE_CURVE ( 'NONE', #12916, #17567, #15813, .T. ) ;
#14749=CARTESIAN_POINT ( 'NONE',  ( 2.000000000000000000, 2.449293598294706414E-16, 0.4999999999999995559 ) ) ;
#14750=DIRECTION ( 'NONE',  ( 1.000000000000000000, 0.000000000000000000, 0.000000000000000000 ) ) ;
#14771=VERTEX_POINT ( 'NONE', #12053 ) ;
#14994=DIRECTION ( 'NONE',  ( 1.000000000000000000, 0.000000000000000000, 0.000000000000000000 ) ) ;
#15053=PRODUCT_CONTEXT ( 'NONE', #16939, 'mechanical' ) ;
#15252=EDGE_CURVE ( 'NONE', #17567, #12916, #3708, .T. ) ;
#15290=SHAPE_REPRESENTATION ( 'Pin 4X6', ( #8005 ), #13887 ) ;
#15410=EDGE_LOOP ( 'NONE', ( #10532, #1940 ) ) ;
#15539=ORIENTED_EDGE ( 'NONE', *, *, #9905, .T. ) ;
#15813=CIRCLE ( 'NONE', #9182, 1.499999999999998668 ) ;
#16184=( GEOMETRIC_REPRESENTATION_CONTEXT ( 3 ) GLOBAL_UNCERTAINTY_ASSIGNED_CONTEXT ( ( #22551 ) ) GLOBAL_UNIT_ASSIGNED_CONTEXT ( ( #5601, #1827, #20606 ) ) REPRESENTATION_CONTEXT ( 'NONE', 'WORKASPACE' ) );
#16228=PRODUCT_DEFINITION_FORMATION_WITH_SPECIFIED_SOURCE ( 'ANY', '', #3416, .NOT_KNOWN. ) ;
#16295=DIRECTION ( 'NONE',  ( 0.000000000000000000, 0.000000000000000000, 1.000000000000000000 ) ) ;
#16404=FACE_OUTER_BOUND ( 'NONE', #13708, .T. ) ;
#16463=CIRCLE ( 'NONE', #5955, 2.000000000000000000 ) ;
#16655=ORIENTED_EDGE ( 'NONE', *, *, #8221, .F. ) ;
#16789=CIRCLE ( 'NONE', #6285, 2.000000000000000000 ) ;
#16819=VECTOR ( 'NONE', #22210, 1000.000000000000000 ) ;
#16921=ORIENTED_EDGE ( 'NONE', *, *, #8221, .T. ) ;
#16939=APPLICATION_CONTEXT ( 'automotive_design' ) ;
#17072=AXIS2_PLACEMENT_3D ( 'NONE', #14581, #16295, #23755 ) ;
#17102=ADVANCED_FACE ( 'NONE', ( #3868 ), #11274, .F. ) ;
#17263=DIRECTION ( 'NONE',  ( -0.000000000000000000, -0.000000000000000000, -1.000000000000000000 ) ) ;
#17567=VERTEX_POINT ( 'NONE', #65 ) ;
#17731=LINE ( 'NONE', #1148, #13169 ) ;
#18103=DIRECTION ( 'NONE',  ( -0.000000000000000000, -0.000000000000000000, -1.000000000000000000 ) ) ;
#18134=DIRECTION ( 'NONE',  ( 0.000000000000000000, 0.000000000000000000, -1.000000000000000000 ) ) ;
#18480=LINE ( 'NONE', #7129, #19948 ) ;
#18578=ORIENTED_EDGE ( 'NONE', *, *, #3201, .T. ) ;
#18634=DIRECTION ( 'NONE',  ( -0.000000000000000000, -0.000000000000000000, 1.000000000000000000 ) ) ;
#18864=CYLINDRICAL_SURFACE ( 'NONE', #20201, 2.000000000000000000 ) ;
#18906=DIRECTION ( 'NONE',  ( 0.000000000000000000, 0.000000000000000000, 1.000000000000000000 ) ) ;
#18910=ORIENTED_EDGE ( 'NONE', *, *, #22646, .F. ) ;
#18991=DIRECTION ( 'NONE',  ( -0.000000000000000000, -0.000000000000000000, -1.000000000000000000 ) ) ;
#19005=CARTESIAN_POINT ( 'NONE',  ( 0.000000000000000000, 0.000000000000000000, 0.000000000000000000 ) ) ;
#19071=CARTESIAN_POINT ( 'NONE',  ( -2.000000000000000000, 2.449293598294706414E-16, 0.4999999999999995559 ) ) ;
#19283=LINE ( 'NONE', #5979, #22378 ) ;
#19335=DIRECTION ( 'NONE',  ( -0.000000000000000000, -0.000000000000000000, 1.000000000000000000 ) ) ;
#19603=CARTESIAN_POINT ( 'NONE',  ( 1.499999999999999556, 2.143131898507867804E-16, 6.000000000000000000 ) ) ;
#19705=FACE_OUTER_BOUND ( 'NONE', #3470, .T. ) ;
#19744=AXIS2_PLACEMENT_3D ( 'NONE', #2144, #18991, #5921 ) ;
#19943=ORIENTED_EDGE ( 'NONE', *, *, #22646, .T. ) ;
#19948=VECTOR ( 'NONE', #5538, 1000.000000000000000 ) ;
#19969=AXIS2_PLACEMENT_3D ( 'NONE', #21520, #4690, #1399 ) ;
#20031=CONICAL_SURFACE ( 'NONE', #19969, 1.499999999999999556, 0.7853981633974457255 ) ;
#20098=FACE_OUTER_BOUND ( 'NONE', #8690, .T. ) ;
#20201=AXIS2_PLACEMENT_3D ( 'NONE', #5923, #17263, #4108 ) ;
#20216=CARTESIAN_POINT ( 'NONE',  ( 0.000000000000000000, 0.000000000000000000, 0.4999999999999995559 ) ) ;
#20306=EDGE_CURVE ( 'NONE', #3333, #10964, #554, .T. ) ;
#20377=CIRCLE ( 'NONE', #6747, 2.000000000000000000 ) ;
#20441=AXIS2_PLACEMENT_3D ( 'NONE', #22055, #7377, #22279 ) ;
#20478=( LENGTH_UNIT ( ) NAMED_UNIT ( * ) SI_UNIT ( .MILLI., .METRE. ) );
#20606=( NAMED_UNIT ( * ) SI_UNIT ( $, .STERADIAN. ) SOLID_ANGLE_UNIT ( ) );
#20750=ORIENTED_EDGE ( 'NONE', *, *, #10720, .F. ) ;
#20875=DIRECTION ( 'NONE',  ( 0.7071067811865456854, 8.659560562354910671E-17, -0.7071067811865493491 ) ) ;
#21520=CARTESIAN_POINT ( 'NONE',  ( 0.000000000000000000, 0.000000000000000000, 6.000000000000000000 ) ) ;
#21699=DIRECTION ( 'NONE',  ( 0.7071067811865489050, 0.000000000000000000, 0.7071067811865462405 ) ) ;
#22049=AXIS2_PLACEMENT_3D ( 'NONE', #14007, #1090, #8615 ) ;
#22055=CARTESIAN_POINT ( 'NONE',  ( 0.000000000000000000, 0.000000000000000000, 0.000000000000000000 ) ) ;
#22210=DIRECTION ( 'NONE',  ( -0.000000000000000000, -0.000000000000000000, -1.000000000000000000 ) ) ;
#22274=SHAPE_DEFINITION_REPRESENTATION ( #6918, #15290 ) ;
#22279=DIRECTION ( 'NONE',  ( 1.000000000000000000, 0.000000000000000000, 0.000000000000000000 ) ) ;
#22344=DIRECTION ( 'NONE',  ( 0.000000000000000000, 0.000000000000000000, 1.000000000000000000 ) ) ;
#22378=VECTOR ( 'NONE', #20875, 1000.000000000000000 ) ;
#22430=ADVANCED_BREP_SHAPE_REPRESENTATION ( '', ( #2929, #8005 ), #13887 ) ;
#22551=UNCERTAINTY_MEASURE_WITH_UNIT (LENGTH_MEASURE( 1.000000000000000082E-05 ), #5601, 'distance_accuracy_value', 'NONE');
#22571=DIRECTION ( 'NONE',  ( -0.000000000000000000, -0.000000000000000000, 1.000000000000000000 ) ) ;
#22639=FACE_OUTER_BOUND ( 'NONE', #7897, .T. ) ;
#22646=EDGE_CURVE ( 'NONE', #12916, #780, #6014, .T. ) ;
#23085=AXIS2_PLACEMENT_3D ( 'NONE', #6637, #19335, #10409 ) ;
#23120=ORIENTED_EDGE ( 'NONE', *, *, #10720, .T. ) ;
#23525=ADVANCED_FACE ( 'NONE', ( #22639 ), #5562, .T. ) ;
#23739=CARTESIAN_POINT ( 'NONE',  ( 0.000000000000000000, 0.000000000000000000, 0.000000000000000000 ) ) ;
#23755=DIRECTION ( 'NONE',  ( 1.000000000000000000, 0.000000000000000000, -0.000000000000000000 ) ) ;
#23844=DIRECTION ( 'NONE',  ( 1.000000000000000000, 0.000000000000000000, 0.000000000000000000 ) ) ;
#24035=DIRECTION ( 'NONE',  ( 0.000000000000000000, 0.000000000000000000, -1.000000000000000000 ) ) ;
#24149=COLOUR_RGB('Grey',0.48,0.52,0.57);
#24150=FILL_AREA_STYLE_COLOUR('',#24149);
#24151=FILL_AREA_STYLE('',(#24150));
#24152=SURFACE_STYLE_FILL_AREA(#24151);
#24153=SURFACE_SIDE_STYLE('',(#24152));
#24154=SURFACE_STYLE_USAGE(.BOTH.,#24153);
#24155=PRESENTATION_STYLE_ASSIGNMENT((#24154));
ENDSEC;
END-ISO-10303-21;
